ISO-10303-21;
HEADER;
FILE_DESCRIPTION (('STEP AP214'),
    '1' );
FILE_NAME ('socket head cap screw_iso_ISO 4762 M5 x 16 - 16N.step',
    '2026-10-03T12:29:21',
    ( '' ),
    ( '' ),
    'SwSTEP 2.0',
    'SolidWorks 2026',
    '' );
FILE_SCHEMA (( 'AUTOMOTIVE_DESIGN' ));
ENDSEC;

DATA;
#74=DIRECTION ( 'NONE',  ( 0.000000000000000000, 0.4999999999999990008, -0.8660254037844391517 ) ) ;
#78=TOROIDAL_SURFACE ( 'NONE', #2431, 2.700000000000000622, 0.2000000000000000111 ) ;
#124=ORIENTED_EDGE ( 'NONE', *, *, #20626, .F. ) ;
#133=ORIENTED_EDGE ( 'NONE', *, *, #9590, .F. ) ;
#164=CARTESIAN_POINT ( 'NONE',  ( 21.00000000000000355, 2.516649172247811061E-16, -2.055000000000000160 ) ) ;
#185=DIRECTION ( 'NONE',  ( 1.000000000000000000, 0.000000000000000000, 0.000000000000000000 ) ) ;
#196=DIRECTION ( 'NONE',  ( -1.000000000000000000, -0.000000000000000000, -0.000000000000000000 ) ) ;
#202=DIRECTION ( 'NONE',  ( 0.000000000000000000, 0.8660254037844380415, -0.5000000000000012212 ) ) ;
#248=ORIENTED_EDGE ( 'NONE', *, *, #5986, .F. ) ;
#252=DIRECTION ( 'NONE',  ( -1.000000000000000000, -0.000000000000000000, -0.000000000000000000 ) ) ;
#253=VECTOR ( 'NONE', #13446, 1000.000000000000000 ) ;
#278=EDGE_LOOP ( 'NONE', ( #9863, #20923 ) ) ;
#298=DIRECTION ( 'NONE',  ( -1.000000000000000000, -0.000000000000000000, -0.000000000000000000 ) ) ;
#312=ADVANCED_FACE ( 'NONE', ( #5902 ), #17141, .T. ) ;
#329=CARTESIAN_POINT ( 'NONE',  ( -31.74999999999995737, 3.061616997868383634E-16, -2.500000000000000444 ) ) ;
#345=ORIENTED_EDGE ( 'NONE', *, *, #11654, .T. ) ;
#366=EDGE_CURVE ( 'NONE', #1598, #19691, #9182, .T. ) ;
#371=CARTESIAN_POINT ( 'NONE',  ( 2.500000000000000000, 2.629050547790028946E-15, 2.042000000000000259 ) ) ;
#390=ADVANCED_FACE ( 'NONE', ( #4205 ), #11548, .F. ) ;
#399=EDGE_CURVE ( 'NONE', #15833, #20459, #9087, .T. ) ;
#401=VECTOR ( 'NONE', #13393, 1000.000000000000000 ) ;
#417=ADVANCED_FACE ( 'NONE', ( #11194 ), #8420, .T. ) ;
#435=ORIENTED_EDGE ( 'NONE', *, *, #9307, .T. ) ;
#440=VERTEX_POINT ( 'NONE', #3545 ) ;
#444=AXIS2_PLACEMENT_3D ( 'NONE', #3077, #18985, #4249 ) ;
#445=ADVANCED_FACE ( 'NONE', ( #16181 ), #20833, .T. ) ;
#464=CARTESIAN_POINT ( 'NONE',  ( 2.500000000000000000, 1.178949249685212974, -2.042000000000001148 ) ) ;
#483=CARTESIAN_POINT ( 'NONE',  ( 3.678949249685231848, 0.000000000000000000, 0.000000000000000000 ) ) ;
#510=VERTEX_POINT ( 'NONE', #11579 ) ;
#540=VERTEX_POINT ( 'NONE', #14767 ) ;
#588=VERTEX_POINT ( 'NONE', #20812 ) ;
#606=CARTESIAN_POINT ( 'NONE',  ( 2.500000000000000000, 0.000000000000000000, 0.000000000000000000 ) ) ;
#617=LINE ( 'NONE', #825, #17851 ) ;
#630=FILL_AREA_STYLE_COLOUR ( '', #18791 ) ;
#644=ORIENTED_EDGE ( 'NONE', *, *, #7272, .T. ) ;
#669=FACE_OUTER_BOUND ( 'NONE', #3773, .T. ) ;
#713=CARTESIAN_POINT ( 'NONE',  ( 0.2500000000000002220, 0.000000000000000000, 0.000000000000000000 ) ) ;
#730=EDGE_CURVE ( 'NONE', #14616, #3271, #16555, .T. ) ;
#747=ORIENTED_EDGE ( 'NONE', *, *, #9656, .T. ) ;
#759=CARTESIAN_POINT ( 'NONE',  ( 4.999999999999997335, 5.204748896376250699E-16, -4.250000000000000000 ) ) ;
#771=DIRECTION ( 'NONE',  ( 0.000000000000000000, -1.287488025362403787E-15, -1.000000000000000000 ) ) ;
#779=AXIS2_PLACEMENT_3D ( 'NONE', #17662, #11494, #3132 ) ;
#825=CARTESIAN_POINT ( 'NONE',  ( 2.500000000000000000, -1.178949249685214307, 2.042000000000001592 ) ) ;
#861=EDGE_CURVE ( 'NONE', #20459, #14616, #12427, .T. ) ;
#887=ADVANCED_FACE ( 'NONE', ( #18899 ), #2880, .F. ) ;
#896=VERTEX_POINT ( 'NONE', #17088 ) ;
#898=TOROIDAL_SURFACE ( 'NONE', #13427, 2.700000000000000622, 0.2000000000000000111 ) ;
#911=EDGE_LOOP ( 'NONE', ( #2651, #5379, #14973 ) ) ;
#913=CIRCLE ( 'NONE', #2266, 0.2000000000000000944 ) ;
#959=ORIENTED_EDGE ( 'NONE', *, *, #13129, .F. ) ;
#966=DIRECTION ( 'NONE',  ( 1.000000000000000000, 0.000000000000000000, 0.000000000000000000 ) ) ;
#1014=PLANE ( 'NONE',  #4630 ) ;
#1022=DIRECTION ( 'NONE',  ( 0.000000000000000000, 0.000000000000000000, 1.000000000000000000 ) ) ;
#1031=DIRECTION ( 'NONE',  ( 0.000000000000000000, -0.4999999999999993339, 0.8660254037844390407 ) ) ;
#1076=DIRECTION ( 'NONE',  ( -1.000000000000000000, -0.000000000000000000, -0.000000000000000000 ) ) ;
#1097=ORIENTED_EDGE ( 'NONE', *, *, #18827, .T. ) ;
#1100=FACE_OUTER_BOUND ( 'NONE', #13056, .T. ) ;
#1175=AXIS2_PLACEMENT_3D ( 'NONE', #13507, #18591, #15511 ) ;
#1179=PLANE ( 'NONE',  #12072 ) ;
#1278=AXIS2_PLACEMENT_3D ( 'NONE', #13562, #5291, #10487 ) ;
#1298=VERTEX_POINT ( 'NONE', #9008 ) ;
#1314=ORIENTED_EDGE ( 'NONE', *, *, #11453, .F. ) ;
#1324=PLANE ( 'NONE',  #12771 ) ;
#1325=CARTESIAN_POINT ( 'NONE',  ( 2.500000000000000000, 1.178949249685212974, -2.042000000000001148 ) ) ;
#1383=FACE_OUTER_BOUND ( 'NONE', #4278, .T. ) ;
#1386=ORIENTED_EDGE ( 'NONE', *, *, #9656, .F. ) ;
#1426=EDGE_LOOP ( 'NONE', ( #6656, #5108, #124, #16239 ) ) ;
#1441=ORIENTED_EDGE ( 'NONE', *, *, #9365, .F. ) ;
#1475=COLOUR_RGB ( '', 0.09019608, 0.27058824, 0.51372549) ;
#1486=CIRCLE ( 'NONE', #5867, 2.700000000000000622 ) ;
#1493=DIRECTION ( 'NONE',  ( 0.000000000000000000, 0.000000000000000000, 1.000000000000000000 ) ) ;
#1499=CARTESIAN_POINT ( 'NONE',  ( 2.500000000000000000, 2.357898499370431722, -2.818925648462311528E-15 ) ) ;
#1575=CARTESIAN_POINT ( 'NONE',  ( 5.000000000000002665, 3.306546357697854226E-16, 2.700000000000000622 ) ) ;
#1578=ADVANCED_FACE ( 'NONE', ( #9431, #1383 ), #14312, .T. ) ;
#1580=EDGE_CURVE ( 'NONE', #3802, #19413, #19723, .T. ) ;
#1598=VERTEX_POINT ( 'NONE', #16907 ) ;
#1657=DIRECTION ( 'NONE',  ( -1.000000000000000000, -0.000000000000000000, -0.000000000000000000 ) ) ;
#1690=EDGE_CURVE ( 'NONE', #19413, #3802, #9231, .T. ) ;
#1691=ORIENTED_EDGE ( 'NONE', *, *, #6877, .F. ) ;
#1695=ORIENTED_EDGE ( 'NONE', *, *, #1690, .F. ) ;
#1768=SURFACE_STYLE_FILL_AREA ( #19880 ) ;
#1818=VECTOR ( 'NONE', #4905, 1000.000000000000000 ) ;
#1828=AXIS2_PLACEMENT_3D ( 'NONE', #19837, #10095, #11683 ) ;
#1877=SHAPE_DEFINITION_REPRESENTATION ( #5771, #12383 ) ;
#1934=CIRCLE ( 'NONE', #1278, 2.500000000000000444 ) ;
#1953=ORIENTED_EDGE ( 'NONE', *, *, #10892, .T. ) ;
#2050=EDGE_CURVE ( 'NONE', #14215, #14337, #17033, .T. ) ;
#2065=CARTESIAN_POINT ( 'NONE',  ( 2.500000000000000000, -1.178949249685214307, 2.042000000000001592 ) ) ;
#2073=APPLICATION_CONTEXT ( 'automotive_design' ) ;
#2091=ORIENTED_EDGE ( 'NONE', *, *, #730, .F. ) ;
#2099=FACE_OUTER_BOUND ( 'NONE', #7677, .T. ) ;
#2115=EDGE_CURVE ( 'NONE', #5814, #14337, #16026, .T. ) ;
#2120=ORIENTED_EDGE ( 'NONE', *, *, #366, .F. ) ;
#2134=ADVANCED_FACE ( 'NONE', ( #19745 ), #3629, .F. ) ;
#2145=FACE_OUTER_BOUND ( 'NONE', #6074, .T. ) ;
#2159=VECTOR ( 'NONE', #9655, 999.9999999999997726 ) ;
#2199=CLOSED_SHELL ( 'NONE', ( #8939, #10001, #2881, #15044, #4425, #417, #1578, #445, #7289, #14821, #19003, #312, #11673, #4173, #5444, #9408, #16489, #13775, #2134, #6198, #11800, #19754, #8038, #11525, #887, #4962, #390 ) ) ;
#2237=VECTOR ( 'NONE', #6617, 1000.000000000000114 ) ;
#2266=AXIS2_PLACEMENT_3D ( 'NONE', #2316, #10476, #8769 ) ;
#2276=ORIENTED_EDGE ( 'NONE', *, *, #4160, .T. ) ;
#2316=CARTESIAN_POINT ( 'NONE',  ( 5.200000000000002842, 0.000000000000000000, -2.700000000000000622 ) ) ;
#2361=DIRECTION ( 'NONE',  ( -1.000000000000000000, -0.000000000000000000, -0.000000000000000000 ) ) ;
#2381=DIRECTION ( 'NONE',  ( 0.000000000000000000, 0.000000000000000000, -1.000000000000000000 ) ) ;
#2405=CARTESIAN_POINT ( 'NONE',  ( 0.2500000000000002220, 0.000000000000000000, 4.250000000000000000 ) ) ;
#2418=( NAMED_UNIT ( * ) SI_UNIT ( $, .STERADIAN. ) SOLID_ANGLE_UNIT ( ) );
#2420=UNCERTAINTY_MEASURE_WITH_UNIT (LENGTH_MEASURE( 1.000000000000000082E-05 ), #14805, 'distance_accuracy_value', 'NONE');
#2431=AXIS2_PLACEMENT_3D ( 'NONE', #5821, #12297, #18770 ) ;
#2468=STYLED_ITEM ( 'NONE', ( #11505 ), #3497 ) ;
#2470=CARTESIAN_POINT ( 'NONE',  ( 2.500000000000000000, 2.357898499370431722, -2.818925648462311528E-15 ) ) ;
#2498=ORIENTED_EDGE ( 'NONE', *, *, #1580, .T. ) ;
#2581=DIRECTION ( 'NONE',  ( -1.000000000000000000, -0.000000000000000000, -0.000000000000000000 ) ) ;
#2587=( GEOMETRIC_REPRESENTATION_CONTEXT ( 3 ) GLOBAL_UNCERTAINTY_ASSIGNED_CONTEXT ( ( #18321 ) ) GLOBAL_UNIT_ASSIGNED_CONTEXT ( ( #13661, #7498, #2418 ) ) REPRESENTATION_CONTEXT ( 'NONE', 'WORKASPACE' ) );
#2589=DIRECTION ( 'NONE',  ( -1.000000000000000000, -0.000000000000000000, -0.000000000000000000 ) ) ;
#2598=EDGE_LOOP ( 'NONE', ( #5245, #15939, #1097, #5912 ) ) ;
#2614=CARTESIAN_POINT ( 'NONE',  ( 2.500000000000000000, 1.178949249685212974, -2.042000000000001148 ) ) ;
#2628=DIRECTION ( 'NONE',  ( 0.000000000000000000, 0.000000000000000000, 1.000000000000000000 ) ) ;
#2651=ORIENTED_EDGE ( 'NONE', *, *, #399, .F. ) ;
#2746=FACE_OUTER_BOUND ( 'NONE', #9484, .T. ) ;
#2774=CARTESIAN_POINT ( 'NONE',  ( 2.500000000000000000, 2.357898499370431722, -2.818925648462311528E-15 ) ) ;
#2845=AXIS2_PLACEMENT_3D ( 'NONE', #17316, #15610, #20491 ) ;
#2880=PLANE ( 'NONE',  #15289 ) ;
#2881=ADVANCED_FACE ( 'NONE', ( #7514 ), #78, .F. ) ;
#2948=EDGE_CURVE ( 'NONE', #15833, #13416, #11018, .T. ) ;
#2979=LINE ( 'NONE', #15689, #11376 ) ;
#3077=CARTESIAN_POINT ( 'NONE',  ( 0.2500000000000002220, 0.000000000000000000, 0.000000000000000000 ) ) ;
#3089=AXIS2_PLACEMENT_3D ( 'NONE', #8275, #3498, #16138 ) ;
#3106=CARTESIAN_POINT ( 'NONE',  ( 0.000000000000000000, -1.178949249685214307, 2.042000000000001592 ) ) ;
#3124=EDGE_CURVE ( 'NONE', #6246, #13015, #13974, .T. ) ;
#3132=DIRECTION ( 'NONE',  ( 0.000000000000000000, 0.5000000000000009992, 0.8660254037844380415 ) ) ;
#3179=CARTESIAN_POINT ( 'NONE',  ( 5.000000000000002665, 0.000000000000000000, -2.700000000000000622 ) ) ;
#3183=CIRCLE ( 'NONE', #2845, 0.2500000000000002220 ) ;
#3197=EDGE_LOOP ( 'NONE', ( #10519, #16434, #13543, #5712, #6919 ) ) ;
#3237=PLANE ( 'NONE',  #779 ) ;
#3242=CARTESIAN_POINT ( 'NONE',  ( 5.200000000000002842, 0.000000000000000000, 0.000000000000000000 ) ) ;
#3250=CIRCLE ( 'NONE', #18829, 2.041999999999999815 ) ;
#3254=CARTESIAN_POINT ( 'NONE',  ( 2.500000000000000000, -2.357898499370432166, 3.035766082959412415E-15 ) ) ;
#3271=VERTEX_POINT ( 'NONE', #13011 ) ;
#3310=CYLINDRICAL_SURFACE ( 'NONE', #14265, 2.500000000000000444 ) ;
#3325=EDGE_LOOP ( 'NONE', ( #16902, #6501, #18915, #14151, #7043 ) ) ;
#3344=CARTESIAN_POINT ( 'NONE',  ( -31.74999999999995737, 0.000000000000000000, 0.000000000000000000 ) ) ;
#3361=DIRECTION ( 'NONE',  ( 0.000000000000000000, 0.000000000000000000, 1.000000000000000000 ) ) ;
#3399=PLANE ( 'NONE',  #5982 ) ;
#3473=ORIENTED_EDGE ( 'NONE', *, *, #15735, .T. ) ;
#3486=CARTESIAN_POINT ( 'NONE',  ( 2.500000000000000000, 0.000000000000000000, 0.000000000000000000 ) ) ;
#3497=MANIFOLD_SOLID_BREP ( 'Hex', #2199 ) ;
#3498=DIRECTION ( 'NONE',  ( -1.000000000000000000, -0.000000000000000000, -0.000000000000000000 ) ) ;
#3545=CARTESIAN_POINT ( 'NONE',  ( 21.00000000000000355, 2.789133085058097101E-16, -2.055000000000000160 ) ) ;
#3547=FACE_OUTER_BOUND ( 'NONE', #5763, .T. ) ;
#3552=( NAMED_UNIT ( * ) SI_UNIT ( $, .STERADIAN. ) SOLID_ANGLE_UNIT ( ) );
#3586=CARTESIAN_POINT ( 'NONE',  ( 2.500000000000000000, 2.357898499370431722, -2.818925648462311528E-15 ) ) ;
#3605=FACE_OUTER_BOUND ( 'NONE', #2598, .T. ) ;
#3607=ORIENTED_EDGE ( 'NONE', *, *, #6706, .F. ) ;
#3611=CIRCLE ( 'NONE', #17532, 2.500000000000000888 ) ;
#3629=PLANE ( 'NONE',  #9594 ) ;
#3635=EDGE_CURVE ( 'NONE', #13015, #1598, #13898, .T. ) ;
#3731=FACE_BOUND ( 'NONE', #5116, .T. ) ;
#3751=ORIENTED_EDGE ( 'NONE', *, *, #1690, .T. ) ;
#3773=EDGE_LOOP ( 'NONE', ( #1695, #19820 ) ) ;
#3802=VERTEX_POINT ( 'NONE', #759 ) ;
#3810=CONICAL_SURFACE ( 'NONE', #6181, 2.041999999999999815, 1.047197551196591858 ) ;
#3834=EDGE_CURVE ( 'NONE', #20459, #19592, #14902, .T. ) ;
#3835=VECTOR ( 'NONE', #20140, 1000.000000000000114 ) ;
#3863=VERTEX_POINT ( 'NONE', #11588 ) ;
#4036=DIRECTION ( 'NONE',  ( 0.000000000000000000, -0.4999999999999993339, 0.8660254037844390407 ) ) ;
#4047=ORIENTED_EDGE ( 'NONE', *, *, #14962, .F. ) ;
#4052=CARTESIAN_POINT ( 'NONE',  ( 2.500000000000000000, -1.178949249685214307, 2.042000000000001592 ) ) ;
#4154=TOROIDAL_SURFACE ( 'NONE', #444, 4.000000000000000000, 0.2500000000000000000 ) ;
#4160=EDGE_CURVE ( 'NONE', #19413, #13015, #10425, .T. ) ;
#4173=ADVANCED_FACE ( 'NONE', ( #1100 ), #9827, .T. ) ;
#4196=CIRCLE ( 'NONE', #1175, 4.250000000000000000 ) ;
#4205=FACE_OUTER_BOUND ( 'NONE', #18159, .T. ) ;
#4216=ORIENTED_EDGE ( 'NONE', *, *, #7272, .F. ) ;
#4223=PRESENTATION_STYLE_ASSIGNMENT (( #7073 ) ) ;
#4241=DIRECTION ( 'NONE',  ( -1.000000000000000000, -0.000000000000000000, -0.000000000000000000 ) ) ;
#4249=DIRECTION ( 'NONE',  ( 0.000000000000000000, 0.000000000000000000, 1.000000000000000000 ) ) ;
#4278=EDGE_LOOP ( 'NONE', ( #14531, #10386 ) ) ;
#4351=CARTESIAN_POINT ( 'NONE',  ( 2.500000000000000000, 2.500728763858895382E-16, -2.041999999999999815 ) ) ;
#4364=ORIENTED_EDGE ( 'NONE', *, *, #6372, .T. ) ;
#4366=ORIENTED_EDGE ( 'NONE', *, *, #9307, .F. ) ;
#4372=DIRECTION ( 'NONE',  ( -1.000000000000000000, -0.000000000000000000, -0.000000000000000000 ) ) ;
#4378=CARTESIAN_POINT ( 'NONE',  ( 5.000000000000000888, 4.250000000000000000, 0.000000000000000000 ) ) ;
#4406=EDGE_CURVE ( 'NONE', #13080, #16803, #11666, .T. ) ;
#4411=CARTESIAN_POINT ( 'NONE',  ( 2.500000000000000000, 0.000000000000000000, 0.000000000000000000 ) ) ;
#4425=ADVANCED_FACE ( 'NONE', ( #3605 ), #3310, .T. ) ;
#4433=EDGE_CURVE ( 'NONE', #440, #896, #5448, .T. ) ;
#4522=PLANE ( 'NONE',  #14453 ) ;
#4616=VECTOR ( 'NONE', #16076, 1000.000000000000114 ) ;
#4630=AXIS2_PLACEMENT_3D ( 'NONE', #16905, #16688, #2381 ) ;
#4654=EDGE_CURVE ( 'NONE', #16659, #540, #12299, .T. ) ;
#4692=CARTESIAN_POINT ( 'NONE',  ( 0.2500000000000002220, 0.000000000000000000, 0.000000000000000000 ) ) ;
#4776=AXIS2_PLACEMENT_3D ( 'NONE', #14795, #17880, #17775 ) ;
#4817=EDGE_CURVE ( 'NONE', #7659, #9981, #9874, .T. ) ;
#4832=DIRECTION ( 'NONE',  ( -1.000000000000000000, -0.000000000000000000, -0.000000000000000000 ) ) ;
#4842=AXIS2_PLACEMENT_3D ( 'NONE', #12724, #19177, #17594 ) ;
#4905=DIRECTION ( 'NONE',  ( 0.000000000000000000, 1.000000000000000000, -1.287488025362403787E-15 ) ) ;
#4962=ADVANCED_FACE ( 'NONE', ( #2099 ), #10365, .F. ) ;
#5001=CARTESIAN_POINT ( 'NONE',  ( 2.500000000000000000, -1.178949249685218748, -2.041999999999998039 ) ) ;
#5029=CARTESIAN_POINT ( 'NONE',  ( -31.74999999999995737, 5.204748896376250699E-16, -4.250000000000000000 ) ) ;
#5041=FILL_AREA_STYLE_COLOUR ( '', #1475 ) ;
#5048=PRODUCT_CONTEXT ( 'NONE', #2073, 'mechanical' ) ;
#5050=ORIENTED_EDGE ( 'NONE', *, *, #19311, .F. ) ;
#5082=ORIENTED_EDGE ( 'NONE', *, *, #3834, .T. ) ;
#5108=ORIENTED_EDGE ( 'NONE', *, *, #19311, .T. ) ;
#5116=EDGE_LOOP ( 'NONE', ( #11366, #20273 ) ) ;
#5140=( NAMED_UNIT ( * ) PLANE_ANGLE_UNIT ( ) SI_UNIT ( $, .RADIAN. ) );
#5171=PLANE ( 'NONE',  #19188 ) ;
#5218=CYLINDRICAL_SURFACE ( 'NONE', #1828, 2.500000000000000444 ) ;
#5227=DIRECTION ( 'NONE',  ( 0.000000000000000000, 1.000000000000000000, -1.224646799147353207E-16 ) ) ;
#5245=ORIENTED_EDGE ( 'NONE', *, *, #20626, .T. ) ;
#5284=EDGE_CURVE ( 'NONE', #13416, #3271, #17579, .T. ) ;
#5290=CIRCLE ( 'NONE', #5619, 2.041999999999999815 ) ;
#5291=DIRECTION ( 'NONE',  ( 1.000000000000000000, 0.000000000000000000, 0.000000000000000000 ) ) ;
#5334=DIRECTION ( 'NONE',  ( 0.000000000000000000, 0.000000000000000000, -1.000000000000000000 ) ) ;
#5349=LINE ( 'NONE', #9911, #19172 ) ;
#5353=SURFACE_SIDE_STYLE ('',( #1768 ) ) ;
#5379=ORIENTED_EDGE ( 'NONE', *, *, #6877, .T. ) ;
#5414=CARTESIAN_POINT ( 'NONE',  ( 2.500000000000000000, 1.178949249685217415, 2.041999999999998483 ) ) ;
#5444=ADVANCED_FACE ( 'NONE', ( #12120 ), #16983, .T. ) ;
#5448=CIRCLE ( 'NONE', #3089, 2.055000000000000160 ) ;
#5483=FILL_AREA_STYLE ('',( #630 ) ) ;
#5510=VECTOR ( 'NONE', #18888, 1000.000000000000114 ) ;
#5578=ORIENTED_EDGE ( 'NONE', *, *, #2115, .T. ) ;
#5580=DIRECTION ( 'NONE',  ( 1.000000000000000000, 0.000000000000000000, 0.000000000000000000 ) ) ;
#5619=AXIS2_PLACEMENT_3D ( 'NONE', #15087, #15284, #7224 ) ;
#5654=ORIENTED_EDGE ( 'NONE', *, *, #3124, .T. ) ;
#5712=ORIENTED_EDGE ( 'NONE', *, *, #20634, .F. ) ;
#5727=CARTESIAN_POINT ( 'NONE',  ( 21.00000000000000355, 0.000000000000000000, 2.055000000000000160 ) ) ;
#5734=EDGE_LOOP ( 'NONE', ( #15280, #17496, #14310 ) ) ;
#5760=FACE_OUTER_BOUND ( 'NONE', #14979, .T. ) ;
#5763=EDGE_LOOP ( 'NONE', ( #7249, #17695, #4364, #1441 ) ) ;
#5771=PRODUCT_DEFINITION_SHAPE ( 'NONE', 'NONE',  #17130 ) ;
#5782=VECTOR ( 'NONE', #17182, 1000.000000000000114 ) ;
#5808=CARTESIAN_POINT ( 'NONE',  ( 2.500000000000000000, 1.178949249685212974, -2.042000000000001148 ) ) ;
#5814=VERTEX_POINT ( 'NONE', #19925 ) ;
#5821=CARTESIAN_POINT ( 'NONE',  ( 5.200000000000002842, 0.000000000000000000, 0.000000000000000000 ) ) ;
#5856=( GEOMETRIC_REPRESENTATION_CONTEXT ( 3 ) GLOBAL_UNCERTAINTY_ASSIGNED_CONTEXT ( ( #2420 ) ) GLOBAL_UNIT_ASSIGNED_CONTEXT ( ( #14805, #5140, #3552 ) ) REPRESENTATION_CONTEXT ( 'NONE', 'WORKASPACE' ) );
#5867=AXIS2_PLACEMENT_3D ( 'NONE', #20163, #2589, #10213 ) ;
#5896=ORIENTED_EDGE ( 'NONE', *, *, #4654, .F. ) ;
#5902=FACE_OUTER_BOUND ( 'NONE', #278, .T. ) ;
#5912=ORIENTED_EDGE ( 'NONE', *, *, #13621, .F. ) ;
#5932=DIRECTION ( 'NONE',  ( -1.000000000000000000, -0.000000000000000000, -0.000000000000000000 ) ) ;
#5982=AXIS2_PLACEMENT_3D ( 'NONE', #13265, #6782, #13164 ) ;
#5986=EDGE_CURVE ( 'NONE', #588, #16334, #2979, .T. ) ;
#5996=DIRECTION ( 'NONE',  ( 0.000000000000000000, -0.5000000000000013323, -0.8660254037844380415 ) ) ;
#6008=DIRECTION ( 'NONE',  ( 1.000000000000000000, 0.000000000000000000, 0.000000000000000000 ) ) ;
#6049=CARTESIAN_POINT ( 'NONE',  ( 2.500000000000000000, -1.768423874527823569, 1.021000000000002350 ) ) ;
#6056=ORIENTED_EDGE ( 'NONE', *, *, #11617, .T. ) ;
#6074=EDGE_LOOP ( 'NONE', ( #6251, #12877, #16998, #644 ) ) ;
#6081=CARTESIAN_POINT ( 'NONE',  ( 2.500000000000000000, 1.768423874527822459, -1.021000000000002794 ) ) ;
#6101=CARTESIAN_POINT ( 'NONE',  ( 0.000000000000000000, 0.000000000000000000, 0.000000000000000000 ) ) ;
#6125=ORIENTED_EDGE ( 'NONE', *, *, #5986, .T. ) ;
#6137=VECTOR ( 'NONE', #1031, 1000.000000000000000 ) ;
#6181=AXIS2_PLACEMENT_3D ( 'NONE', #606, #9077, #1022 ) ;
#6198=ADVANCED_FACE ( 'NONE', ( #13147 ), #5171, .F. ) ;
#6246=VERTEX_POINT ( 'NONE', #7070 ) ;
#6249=CARTESIAN_POINT ( 'NONE',  ( 2.500000000000000000, 0.000000000000000000, 0.000000000000000000 ) ) ;
#6251=ORIENTED_EDGE ( 'NONE', *, *, #13780, .F. ) ;
#6303=DIRECTION ( 'NONE',  ( -1.000000000000000000, -0.000000000000000000, -0.000000000000000000 ) ) ;
#6372=EDGE_CURVE ( 'NONE', #15532, #14215, #913, .T. ) ;
#6382=ORIENTED_EDGE ( 'NONE', *, *, #6706, .T. ) ;
#6395=ORIENTED_EDGE ( 'NONE', *, *, #14772, .F. ) ;
#6415=CARTESIAN_POINT ( 'NONE',  ( 2.500000000000000000, 2.357898499370431722, -2.818925648462311528E-15 ) ) ;
#6420=ORIENTED_EDGE ( 'NONE', *, *, #14076, .F. ) ;
#6452=VECTOR ( 'NONE', #2361, 1000.000000000000000 ) ;
#6490=EDGE_LOOP ( 'NONE', ( #4366, #2498, #2276, #6529 ) ) ;
#6501=ORIENTED_EDGE ( 'NONE', *, *, #4654, .T. ) ;
#6529=ORIENTED_EDGE ( 'NONE', *, *, #14962, .T. ) ;
#6533=VECTOR ( 'NONE', #19085, 999.9999999999997726 ) ;
#6558=CIRCLE ( 'NONE', #16061, 2.055000000000000160 ) ;
#6578=CARTESIAN_POINT ( 'NONE',  ( -31.74999999999995737, 0.000000000000000000, 0.000000000000000000 ) ) ;
#6616=DIRECTION ( 'NONE',  ( 0.000000000000000000, 0.000000000000000000, 1.000000000000000000 ) ) ;
#6617=DIRECTION ( 'NONE',  ( -0.7071067811865364705, 8.659560562355067211E-17, -0.7071067811865584529 ) ) ;
#6656=ORIENTED_EDGE ( 'NONE', *, *, #12214, .T. ) ;
#6700=CARTESIAN_POINT ( 'NONE',  ( 2.500000000000000000, 1.178949249685217415, 2.041999999999998483 ) ) ;
#6706=EDGE_CURVE ( 'NONE', #588, #7659, #17788, .T. ) ;
#6725=DIRECTION ( 'NONE',  ( 0.000000000000000000, 1.000000000000000000, -1.287488025362403787E-15 ) ) ;
#6752=ORIENTED_EDGE ( 'NONE', *, *, #3124, .F. ) ;
#6755=DIRECTION ( 'NONE',  ( 0.000000000000000000, 0.000000000000000000, 1.000000000000000000 ) ) ;
#6782=DIRECTION ( 'NONE',  ( -0.000000000000000000, 0.8660254037844392627, 0.4999999999999990008 ) ) ;
#6808=AXIS2_PLACEMENT_3D ( 'NONE', #3344, #4832, #6616 ) ;
#6868=AXIS2_PLACEMENT_3D ( 'NONE', #8497, #5227, #19847 ) ;
#6877=EDGE_CURVE ( 'NONE', #15833, #19592, #7696, .T. ) ;
#6917=CARTESIAN_POINT ( 'NONE',  ( 0.000000000000000000, 2.357898499370431722, -2.818925648462311528E-15 ) ) ;
#6919=ORIENTED_EDGE ( 'NONE', *, *, #10784, .T. ) ;
#6959=LINE ( 'NONE', #11632, #253 ) ;
#7015=EDGE_CURVE ( 'NONE', #19691, #1598, #20213, .T. ) ;
#7043=ORIENTED_EDGE ( 'NONE', *, *, #13593, .T. ) ;
#7054=CARTESIAN_POINT ( 'NONE',  ( 0.000000000000000000, -1.178949249685214307, 2.042000000000001592 ) ) ;
#7070=CARTESIAN_POINT ( 'NONE',  ( 0.2500000000000002220, 5.204748896376250699E-16, -4.250000000000000000 ) ) ;
#7073=SURFACE_STYLE_USAGE ( .BOTH. , #12168 ) ;
#7089=EDGE_LOOP ( 'NONE', ( #6056, #13745, #12262 ) ) ;
#7108=EDGE_LOOP ( 'NONE', ( #10435, #1386, #17226, #16137, #15114, #8921 ) ) ;
#7213=CARTESIAN_POINT ( 'NONE',  ( 2.500000000000000000, -2.357898499370432166, 3.035766082959412415E-15 ) ) ;
#7224=DIRECTION ( 'NONE',  ( 0.000000000000000000, 0.000000000000000000, 1.000000000000000000 ) ) ;
#7249=ORIENTED_EDGE ( 'NONE', *, *, #2115, .F. ) ;
#7272=EDGE_CURVE ( 'NONE', #5814, #15532, #7666, .T. ) ;
#7289=ADVANCED_FACE ( 'NONE', ( #3731, #669 ), #1324, .T. ) ;
#7291=UNCERTAINTY_MEASURE_WITH_UNIT (LENGTH_MEASURE( 1.000000000000000082E-05 ), #16732, 'distance_accuracy_value', 'NONE');
#7327=CARTESIAN_POINT ( 'NONE',  ( 2.500000000000000000, 2.357898499370431722, -2.818925648462311528E-15 ) ) ;
#7339=ORIENTED_EDGE ( 'NONE', *, *, #4406, .T. ) ;
#7395=( NAMED_UNIT ( * ) SI_UNIT ( $, .STERADIAN. ) SOLID_ANGLE_UNIT ( ) );
#7417=ORIENTED_EDGE ( 'NONE', *, *, #3635, .F. ) ;
#7444=DIRECTION ( 'NONE',  ( -1.000000000000000000, -0.000000000000000000, -0.000000000000000000 ) ) ;
#7479=DIRECTION ( 'NONE',  ( -1.000000000000000000, -0.000000000000000000, -0.000000000000000000 ) ) ;
#7498=( NAMED_UNIT ( * ) PLANE_ANGLE_UNIT ( ) SI_UNIT ( $, .RADIAN. ) );
#7511=CARTESIAN_POINT ( 'NONE',  ( 20.55500000000001748, 0.000000000000000000, 0.000000000000000000 ) ) ;
#7514=FACE_OUTER_BOUND ( 'NONE', #13371, .T. ) ;
#7517=LINE ( 'NONE', #14003, #6533 ) ;
#7541=VECTOR ( 'NONE', #18832, 1000.000000000000000 ) ;
#7624=CARTESIAN_POINT ( 'NONE',  ( 2.500000000000000000, 2.357898499370431722, -2.818925648462311528E-15 ) ) ;
#7644=CARTESIAN_POINT ( 'NONE',  ( 2.500000000000000000, -1.178949249685214307, 2.042000000000001592 ) ) ;
#7659=VERTEX_POINT ( 'NONE', #8563 ) ;
#7666=CIRCLE ( 'NONE', #8016, 2.500000000000000444 ) ;
#7677=EDGE_LOOP ( 'NONE', ( #3473, #18980, #6420 ) ) ;
#7696=LINE ( 'NONE', #15853, #14159 ) ;
#7711=CARTESIAN_POINT ( 'NONE',  ( 0.000000000000000000, -2.357898499370432166, 3.035766082959412415E-15 ) ) ;
#7755=DIRECTION ( 'NONE',  ( 1.000000000000000000, 0.000000000000000000, 0.000000000000000000 ) ) ;
#7835=AXIS2_PLACEMENT_3D ( 'NONE', #6101, #7479, #14390 ) ;
#7898=AXIS2_PLACEMENT_3D ( 'NONE', #11891, #8926, #12004 ) ;
#7923=CONICAL_SURFACE ( 'NONE', #13341, 2.055000000000000160, 0.7853981633974639331 ) ;
#7982=VECTOR ( 'NONE', #18990, 1000.000000000000114 ) ;
#8016=AXIS2_PLACEMENT_3D ( 'NONE', #12012, #15192, #5334 ) ;
#8038=ADVANCED_FACE ( 'NONE', ( #10863 ), #10972, .F. ) ;
#8097=EDGE_CURVE ( 'NONE', #11587, #20459, #14292, .T. ) ;
#8275=CARTESIAN_POINT ( 'NONE',  ( 21.00000000000000355, 0.000000000000000000, 0.000000000000000000 ) ) ;
#8348=AXIS2_PLACEMENT_3D ( 'NONE', #6249, #4241, #9531 ) ;
#8420=CYLINDRICAL_SURFACE ( 'NONE', #4776, 4.250000000000000000 ) ;
#8497=CARTESIAN_POINT ( 'NONE',  ( 5.200000000000002842, 3.306546357697854226E-16, 2.700000000000000622 ) ) ;
#8555=DIRECTION ( 'NONE',  ( 0.000000000000000000, 0.000000000000000000, -1.000000000000000000 ) ) ;
#8563=CARTESIAN_POINT ( 'NONE',  ( 2.500000000000000000, -1.768423874527825568, -1.020999999999998575 ) ) ;
#8743=ORIENTED_EDGE ( 'NONE', *, *, #6372, .F. ) ;
#8769=DIRECTION ( 'NONE',  ( 0.000000000000000000, 0.000000000000000000, -1.000000000000000000 ) ) ;
#8842=EDGE_CURVE ( 'NONE', #540, #13080, #13951, .T. ) ;
#8846=EDGE_CURVE ( 'NONE', #9221, #16803, #12365, .T. ) ;
#8921=ORIENTED_EDGE ( 'NONE', *, *, #14150, .F. ) ;
#8926=DIRECTION ( 'NONE',  ( -1.000000000000000000, -0.000000000000000000, -0.000000000000000000 ) ) ;
#8933=DIRECTION ( 'NONE',  ( 0.000000000000000000, -0.8660254037844390407, -0.4999999999999993339 ) ) ;
#8939=ADVANCED_FACE ( 'NONE', ( #17132 ), #3810, .F. ) ;
#9008=CARTESIAN_POINT ( 'NONE',  ( 2.500000000000000000, 1.178949249685212974, -2.042000000000001148 ) ) ;
#9060=CARTESIAN_POINT ( 'NONE',  ( 0.000000000000000000, -1.178949249685218748, -2.041999999999998039 ) ) ;
#9077=DIRECTION ( 'NONE',  ( -1.000000000000000000, -0.000000000000000000, -0.000000000000000000 ) ) ;
#9083=CARTESIAN_POINT ( 'NONE',  ( 0.000000000000000000, -2.357898499370432166, 3.035766082959412415E-15 ) ) ;
#9087=LINE ( 'NONE', #15538, #6137 ) ;
#9182=CIRCLE ( 'NONE', #7835, 4.000000000000000000 ) ;
#9221=VERTEX_POINT ( 'NONE', #19861 ) ;
#9231=CIRCLE ( 'NONE', #13300, 4.250000000000000000 ) ;
#9280=DIRECTION ( 'NONE',  ( 0.000000000000000000, 0.000000000000000000, -1.000000000000000000 ) ) ;
#9307=EDGE_CURVE ( 'NONE', #3802, #6246, #19548, .T. ) ;
#9365=EDGE_CURVE ( 'NONE', #14337, #14215, #1486, .T. ) ;
#9408=ADVANCED_FACE ( 'NONE', ( #13510 ), #12124, .F. ) ;
#9431=FACE_BOUND ( 'NONE', #7108, .T. ) ;
#9484=EDGE_LOOP ( 'NONE', ( #5050, #11448, #12406, #18970 ) ) ;
#9523=CARTESIAN_POINT ( 'NONE',  ( 4.999999999999997335, 0.000000000000000000, 0.000000000000000000 ) ) ;
#9528=AXIS2_PLACEMENT_3D ( 'NONE', #4411, #10681, #2628 ) ;
#9531=DIRECTION ( 'NONE',  ( 0.000000000000000000, 0.000000000000000000, 1.000000000000000000 ) ) ;
#9590=EDGE_CURVE ( 'NONE', #6246, #19691, #3183, .T. ) ;
#9594=AXIS2_PLACEMENT_3D ( 'NONE', #464, #771, #15083 ) ;
#9652=ORIENTED_EDGE ( 'NONE', *, *, #2948, .F. ) ;
#9655=DIRECTION ( 'NONE',  ( 0.000000000000000000, -0.5000000000000013323, -0.8660254037844380415 ) ) ;
#9656=EDGE_CURVE ( 'NONE', #16131, #3271, #17942, .T. ) ;
#9680=CARTESIAN_POINT ( 'NONE',  ( 0.000000000000000000, -1.178949249685214307, 2.042000000000001592 ) ) ;
#9707=FACE_OUTER_BOUND ( 'NONE', #10310, .T. ) ;
#9813=DIRECTION ( 'NONE',  ( 0.000000000000000000, -0.4999999999999993339, 0.8660254037844390407 ) ) ;
#9827=TOROIDAL_SURFACE ( 'NONE', #12210, 4.000000000000000000, 0.2500000000000000000 ) ;
#9860=VECTOR ( 'NONE', #16539, 1000.000000000000000 ) ;
#9863=ORIENTED_EDGE ( 'NONE', *, *, #12214, .F. ) ;
#9874=CIRCLE ( 'NONE', #12597, 2.041999999999999815 ) ;
#9905=AXIS2_PLACEMENT_3D ( 'NONE', #713, #19588, #9940 ) ;
#9911=CARTESIAN_POINT ( 'NONE',  ( 2.500000000000000000, -1.178949249685214307, 2.042000000000001592 ) ) ;
#9940=DIRECTION ( 'NONE',  ( 0.000000000000000000, 0.000000000000000000, 1.000000000000000000 ) ) ;
#9947=CARTESIAN_POINT ( 'NONE',  ( 2.500000000000000000, 2.357898499370431722, -2.818925648462311528E-15 ) ) ;
#9981=VERTEX_POINT ( 'NONE', #6049 ) ;
#9993=ORIENTED_EDGE ( 'NONE', *, *, #4160, .F. ) ;
#10001=ADVANCED_FACE ( 'NONE', ( #18780 ), #4154, .T. ) ;
#10021=STYLED_ITEM ( 'NONE', ( #4223 ), #15250 ) ;
#10095=DIRECTION ( 'NONE',  ( -1.000000000000000000, -0.000000000000000000, -0.000000000000000000 ) ) ;
#10100=CARTESIAN_POINT ( 'NONE',  ( 20.55500000000001748, 0.000000000000000000, 2.500000000000000888 ) ) ;
#10213=DIRECTION ( 'NONE',  ( 0.000000000000000000, 0.000000000000000000, -1.000000000000000000 ) ) ;
#10310=EDGE_LOOP ( 'NONE', ( #12240, #13330, #1953, #345, #6125 ) ) ;
#10342=VECTOR ( 'NONE', #9813, 1000.000000000000000 ) ;
#10365=PLANE ( 'NONE',  #17989 ) ;
#10386=ORIENTED_EDGE ( 'NONE', *, *, #7015, .T. ) ;
#10411=DIRECTION ( 'NONE',  ( 0.000000000000000000, 0.000000000000000000, -1.000000000000000000 ) ) ;
#10425=LINE ( 'NONE', #16886, #6452 ) ;
#10435=ORIENTED_EDGE ( 'NONE', *, *, #5284, .T. ) ;
#10455=DIRECTION ( 'NONE',  ( 0.000000000000000000, -1.000000000000000000, 1.287488025362403787E-15 ) ) ;
#10476=DIRECTION ( 'NONE',  ( 0.000000000000000000, -1.000000000000000000, 0.000000000000000000 ) ) ;
#10487=DIRECTION ( 'NONE',  ( 0.000000000000000000, 0.000000000000000000, -1.000000000000000000 ) ) ;
#10514=EDGE_LOOP ( 'NONE', ( #3607, #13444, #18879 ) ) ;
#10519=ORIENTED_EDGE ( 'NONE', *, *, #8846, .T. ) ;
#10533=DIRECTION ( 'NONE',  ( 0.000000000000000000, -1.000000000000000000, 1.287488025362403787E-15 ) ) ;
#10548=AXIS2_PLACEMENT_3D ( 'NONE', #15646, #12578, #15863 ) ;
#10681=DIRECTION ( 'NONE',  ( -1.000000000000000000, -0.000000000000000000, -0.000000000000000000 ) ) ;
#10727=EDGE_CURVE ( 'NONE', #16131, #16334, #20693, .T. ) ;
#10784=EDGE_CURVE ( 'NONE', #1298, #9221, #10950, .T. ) ;
#10863=FACE_OUTER_BOUND ( 'NONE', #5734, .T. ) ;
#10892=EDGE_CURVE ( 'NONE', #510, #9981, #12316, .T. ) ;
#10950=LINE ( 'NONE', #1325, #12023 ) ;
#10972=PLANE ( 'NONE',  #18329 ) ;
#11018=LINE ( 'NONE', #1499, #17347 ) ;
#11047=ORIENTED_EDGE ( 'NONE', *, *, #399, .T. ) ;
#11101=ORIENTED_EDGE ( 'NONE', *, *, #2050, .F. ) ;
#11179=EDGE_CURVE ( 'NONE', #540, #7659, #3250, .T. ) ;
#11185=AXIS2_PLACEMENT_3D ( 'NONE', #18162, #1657, #19437 ) ;
#11194=FACE_OUTER_BOUND ( 'NONE', #13037, .T. ) ;
#11198=VECTOR ( 'NONE', #19836, 1000.000000000000114 ) ;
#11366=ORIENTED_EDGE ( 'NONE', *, *, #2050, .T. ) ;
#11376=VECTOR ( 'NONE', #1076, 1000.000000000000000 ) ;
#11425=VECTOR ( 'NONE', #14095, 1000.000000000000000 ) ;
#11448=ORIENTED_EDGE ( 'NONE', *, *, #4433, .T. ) ;
#11453=EDGE_CURVE ( 'NONE', #16334, #16803, #15647, .T. ) ;
#11494=DIRECTION ( 'NONE',  ( 0.000000000000000000, 0.8660254037844380415, -0.5000000000000009992 ) ) ;
#11505=PRESENTATION_STYLE_ASSIGNMENT (( #14700 ) ) ;
#11525=ADVANCED_FACE ( 'NONE', ( #17571 ), #4522, .F. ) ;
#11548=CONICAL_SURFACE ( 'NONE', #9528, 2.041999999999999815, 1.047197551196591858 ) ;
#11568=VECTOR ( 'NONE', #4036, 1000.000000000000000 ) ;
#11574=DIRECTION ( 'NONE',  ( 0.000000000000000000, -1.000000000000000000, 0.000000000000000000 ) ) ;
#11579=CARTESIAN_POINT ( 'NONE',  ( 2.500000000000000000, -1.178949249685214307, 2.042000000000001592 ) ) ;
#11582=DIRECTION ( 'NONE',  ( 0.000000000000000000, 0.000000000000000000, 1.000000000000000000 ) ) ;
#11587=VERTEX_POINT ( 'NONE', #371 ) ;
#11588=CARTESIAN_POINT ( 'NONE',  ( 20.55500000000001748, 3.061616997868384127E-16, -2.500000000000000888 ) ) ;
#11617=EDGE_CURVE ( 'NONE', #11587, #14616, #5349, .T. ) ;
#11632=CARTESIAN_POINT ( 'NONE',  ( 2.500000000000000000, -1.178949249685214307, 2.042000000000001592 ) ) ;
#11642=DIRECTION ( 'NONE',  ( 0.000000000000000000, 0.5000000000000011102, 0.8660254037844379305 ) ) ;
#11654=EDGE_CURVE ( 'NONE', #9981, #588, #14694, .T. ) ;
#11666=LINE ( 'NONE', #5001, #9860 ) ;
#11673=ADVANCED_FACE ( 'NONE', ( #3547 ), #898, .F. ) ;
#11683=DIRECTION ( 'NONE',  ( 0.000000000000000000, 0.000000000000000000, 1.000000000000000000 ) ) ;
#11720=CARTESIAN_POINT ( 'NONE',  ( 2.500000000000000000, 1.768423874527823791, 1.020999999999998353 ) ) ;
#11765=AXIS2_PLACEMENT_3D ( 'NONE', #18641, #15360, #20323 ) ;
#11800=ADVANCED_FACE ( 'NONE', ( #5760 ), #1014, .F. ) ;
#11886=ORIENTED_EDGE ( 'NONE', *, *, #2948, .T. ) ;
#11891=CARTESIAN_POINT ( 'NONE',  ( 5.000000000000000888, 0.000000000000000000, 0.000000000000000000 ) ) ;
#12004=DIRECTION ( 'NONE',  ( 0.000000000000000000, 0.000000000000000000, -1.000000000000000000 ) ) ;
#12012=CARTESIAN_POINT ( 'NONE',  ( 5.200000000000002842, 0.000000000000000000, 0.000000000000000000 ) ) ;
#12023=VECTOR ( 'NONE', #7444, 1000.000000000000000 ) ;
#12039=PRODUCT ( 'socket head cap screw_iso_ISO 4762 M5 x 16 - 16N', 'socket head cap screw_iso_ISO 4762 M5 x 16 - 16N', '', ( #5048 ) ) ;
#12072=AXIS2_PLACEMENT_3D ( 'NONE', #7624, #966, #14207 ) ;
#12120=FACE_OUTER_BOUND ( 'NONE', #16564, .T. ) ;
#12121=DIRECTION ( 'NONE',  ( 1.000000000000000000, 0.000000000000000000, 0.000000000000000000 ) ) ;
#12124=PLANE ( 'NONE',  #16693 ) ;
#12168=SURFACE_SIDE_STYLE ('',( #15352 ) ) ;
#12176=DIRECTION ( 'NONE',  ( 0.000000000000000000, 0.000000000000000000, 1.000000000000000000 ) ) ;
#12210=AXIS2_PLACEMENT_3D ( 'NONE', #4692, #4372, #16029 ) ;
#12214=EDGE_CURVE ( 'NONE', #896, #440, #6558, .T. ) ;
#12240=ORIENTED_EDGE ( 'NONE', *, *, #10727, .F. ) ;
#12262=ORIENTED_EDGE ( 'NONE', *, *, #8097, .F. ) ;
#12297=DIRECTION ( 'NONE',  ( 1.000000000000000000, 0.000000000000000000, 0.000000000000000000 ) ) ;
#12299=LINE ( 'NONE', #4351, #5782 ) ;
#12316=LINE ( 'NONE', #7644, #7982 ) ;
#12365=LINE ( 'NONE', #17021, #7541 ) ;
#12383=SHAPE_REPRESENTATION ( 'socket head cap screw_iso_ISO 4762 M5 x 16 - 16N', ( #12461 ), #2587 ) ;
#12403=DIRECTION ( 'NONE',  ( 0.000000000000000000, 0.000000000000000000, 1.000000000000000000 ) ) ;
#12406=ORIENTED_EDGE ( 'NONE', *, *, #18404, .T. ) ;
#12427=LINE ( 'NONE', #2774, #11568 ) ;
#12455=AXIS2_PLACEMENT_3D ( 'NONE', #17561, #6303, #12886 ) ;
#12461=AXIS2_PLACEMENT_3D ( 'NONE', #19474, #3361, #185 ) ;
#12505=DIRECTION ( 'NONE',  ( -1.000000000000000000, -0.000000000000000000, -0.000000000000000000 ) ) ;
#12545=FACE_OUTER_BOUND ( 'NONE', #1426, .T. ) ;
#12578=DIRECTION ( 'NONE',  ( 1.000000000000000000, 0.000000000000000000, 0.000000000000000000 ) ) ;
#12597=AXIS2_PLACEMENT_3D ( 'NONE', #14726, #17810, #6755 ) ;
#12681=DIRECTION ( 'NONE',  ( 1.000000000000000000, 0.000000000000000000, 0.000000000000000000 ) ) ;
#12701=( GEOMETRIC_REPRESENTATION_CONTEXT ( 3 ) GLOBAL_UNCERTAINTY_ASSIGNED_CONTEXT ( ( #7291 ) ) GLOBAL_UNIT_ASSIGNED_CONTEXT ( ( #16732, #15462, #7395 ) ) REPRESENTATION_CONTEXT ( 'NONE', 'WORKASPACE' ) );
#12724=CARTESIAN_POINT ( 'NONE',  ( 0.000000000000000000, 0.000000000000000000, 0.000000000000000000 ) ) ;
#12725=FACE_OUTER_BOUND ( 'NONE', #10514, .T. ) ;
#12740=CARTESIAN_POINT ( 'NONE',  ( 2.500000000000000000, 0.000000000000000000, 2.041999999999999815 ) ) ;
#12771=AXIS2_PLACEMENT_3D ( 'NONE', #4378, #12121, #13924 ) ;
#12794=CONICAL_SURFACE ( 'NONE', #19530, 2.055000000000000160, 0.7853981633974639331 ) ;
#12873=EDGE_LOOP ( 'NONE', ( #6752, #13629, #2120, #7417 ) ) ;
#12877=ORIENTED_EDGE ( 'NONE', *, *, #12894, .T. ) ;
#12886=DIRECTION ( 'NONE',  ( 0.000000000000000000, 0.000000000000000000, 1.000000000000000000 ) ) ;
#12894=EDGE_CURVE ( 'NONE', #3863, #19670, #3611, .T. ) ;
#12920=APPLICATION_CONTEXT ( 'automotive_design' ) ;
#12958=LINE ( 'NONE', #329, #17845 ) ;
#13011=CARTESIAN_POINT ( 'NONE',  ( 0.000000000000000000, 1.178949249685217415, 2.041999999999998483 ) ) ;
#13015=VERTEX_POINT ( 'NONE', #2405 ) ;
#13020=ORIENTED_EDGE ( 'NONE', *, *, #14772, .T. ) ;
#13037=EDGE_LOOP ( 'NONE', ( #3751, #435, #5654, #9993 ) ) ;
#13056=EDGE_LOOP ( 'NONE', ( #133, #4047, #16765, #18617 ) ) ;
#13080=VERTEX_POINT ( 'NONE', #16716 ) ;
#13105=DIRECTION ( 'NONE',  ( 0.000000000000000000, -0.5000000000000009992, -0.8660254037844380415 ) ) ;
#13129=EDGE_CURVE ( 'NONE', #510, #11587, #6959, .T. ) ;
#13147=FACE_OUTER_BOUND ( 'NONE', #17744, .T. ) ;
#13164=DIRECTION ( 'NONE',  ( 0.000000000000000000, -0.4999999999999989453, 0.8660254037844391517 ) ) ;
#13227=DIRECTION ( 'NONE',  ( 0.000000000000000000, 0.000000000000000000, 1.000000000000000000 ) ) ;
#13265=CARTESIAN_POINT ( 'NONE',  ( 2.500000000000000000, -2.357898499370432166, 3.035766082959412415E-15 ) ) ;
#13300=AXIS2_PLACEMENT_3D ( 'NONE', #14824, #298, #13227 ) ;
#13330=ORIENTED_EDGE ( 'NONE', *, *, #19965, .F. ) ;
#13341=AXIS2_PLACEMENT_3D ( 'NONE', #20488, #19008, #15925 ) ;
#13371=EDGE_LOOP ( 'NONE', ( #4216, #5578, #11101, #8743 ) ) ;
#13393=DIRECTION ( 'NONE',  ( -1.000000000000000000, -0.000000000000000000, -0.000000000000000000 ) ) ;
#13416=VERTEX_POINT ( 'NONE', #6917 ) ;
#13421=DIRECTION ( 'NONE',  ( 1.000000000000000000, 0.000000000000000000, 0.000000000000000000 ) ) ;
#13427=AXIS2_PLACEMENT_3D ( 'NONE', #3242, #13421, #16274 ) ;
#13444=ORIENTED_EDGE ( 'NONE', *, *, #11654, .F. ) ;
#13446=DIRECTION ( 'NONE',  ( 0.000000000000000000, 1.000000000000000000, -1.287488025362403787E-15 ) ) ;
#13507=CARTESIAN_POINT ( 'NONE',  ( 0.2500000000000002220, 0.000000000000000000, 0.000000000000000000 ) ) ;
#13510=FACE_OUTER_BOUND ( 'NONE', #18029, .T. ) ;
#13543=ORIENTED_EDGE ( 'NONE', *, *, #8842, .F. ) ;
#13557=AXIS2_PLACEMENT_3D ( 'NONE', #20031, #11574, #10411 ) ;
#13562=CARTESIAN_POINT ( 'NONE',  ( 5.200000000000002842, 0.000000000000000000, 0.000000000000000000 ) ) ;
#13593=EDGE_CURVE ( 'NONE', #9981, #11587, #5290, .T. ) ;
#13621=EDGE_CURVE ( 'NONE', #19670, #5814, #18585, .T. ) ;
#13629=ORIENTED_EDGE ( 'NONE', *, *, #9590, .T. ) ;
#13653=CARTESIAN_POINT ( 'NONE',  ( 2.500000000000000000, 2.357898499370431722, -2.818925648462311528E-15 ) ) ;
#13661=( LENGTH_UNIT ( ) NAMED_UNIT ( * ) SI_UNIT ( .MILLI., .METRE. ) );
#13745=ORIENTED_EDGE ( 'NONE', *, *, #861, .F. ) ;
#13775=ADVANCED_FACE ( 'NONE', ( #17623 ), #3399, .T. ) ;
#13780=EDGE_CURVE ( 'NONE', #3863, #15532, #12958, .T. ) ;
#13898=CIRCLE ( 'NONE', #13557, 0.2500000000000002220 ) ;
#13924=DIRECTION ( 'NONE',  ( 0.000000000000000000, 0.000000000000000000, -1.000000000000000000 ) ) ;
#13951=LINE ( 'NONE', #2614, #16008 ) ;
#13974=CIRCLE ( 'NONE', #9905, 4.250000000000000000 ) ;
#14003=CARTESIAN_POINT ( 'NONE',  ( 0.000000000000000000, 2.357898499370431722, -2.818925648462311528E-15 ) ) ;
#14076=EDGE_CURVE ( 'NONE', #19592, #540, #14788, .T. ) ;
#14095=DIRECTION ( 'NONE',  ( 0.000000000000000000, -1.000000000000000000, 1.287488025362403787E-15 ) ) ;
#14119=VECTOR ( 'NONE', #2581, 1000.000000000000000 ) ;
#14150=EDGE_CURVE ( 'NONE', #13416, #9221, #7517, .T. ) ;
#14151=ORIENTED_EDGE ( 'NONE', *, *, #4817, .T. ) ;
#14159=VECTOR ( 'NONE', #5996, 999.9999999999997726 ) ;
#14184=DIRECTION ( 'NONE',  ( 0.000000000000000000, 0.000000000000000000, -1.000000000000000000 ) ) ;
#14207=DIRECTION ( 'NONE',  ( 0.000000000000000000, 0.000000000000000000, -1.000000000000000000 ) ) ;
#14215=VERTEX_POINT ( 'NONE', #3179 ) ;
#14265=AXIS2_PLACEMENT_3D ( 'NONE', #6578, #18030, #16431 ) ;
#14292=CIRCLE ( 'NONE', #19681, 2.041999999999999815 ) ;
#14310=ORIENTED_EDGE ( 'NONE', *, *, #13593, .F. ) ;
#14312=PLANE ( 'NONE',  #4842 ) ;
#14337=VERTEX_POINT ( 'NONE', #1575 ) ;
#14390=DIRECTION ( 'NONE',  ( 0.000000000000000000, 0.000000000000000000, 1.000000000000000000 ) ) ;
#14453=AXIS2_PLACEMENT_3D ( 'NONE', #6415, #6008, #14184 ) ;
#14467=DIRECTION ( 'NONE',  ( 0.000000000000000000, -0.5000000000000009992, -0.8660254037844380415 ) ) ;
#14471=ORIENTED_EDGE ( 'NONE', *, *, #730, .T. ) ;
#14531=ORIENTED_EDGE ( 'NONE', *, *, #366, .T. ) ;
#14616=VERTEX_POINT ( 'NONE', #6700 ) ;
#14693=LINE ( 'NONE', #164, #2237 ) ;
#14694=LINE ( 'NONE', #2065, #20167 ) ;
#14700=SURFACE_STYLE_USAGE ( .BOTH. , #5353 ) ;
#14726=CARTESIAN_POINT ( 'NONE',  ( 2.500000000000000000, 0.000000000000000000, 0.000000000000000000 ) ) ;
#14767=CARTESIAN_POINT ( 'NONE',  ( 2.500000000000000000, -2.629050547790028551E-15, -2.041999999999999815 ) ) ;
#14770=CARTESIAN_POINT ( 'NONE',  ( 21.00000000000000355, 0.000000000000000000, 0.000000000000000000 ) ) ;
#14772=EDGE_CURVE ( 'NONE', #7659, #13080, #19934, .T. ) ;
#14788=CIRCLE ( 'NONE', #8348, 2.041999999999999815 ) ;
#14795=CARTESIAN_POINT ( 'NONE',  ( -31.74999999999995737, 0.000000000000000000, 0.000000000000000000 ) ) ;
#14800=ORIENTED_EDGE ( 'NONE', *, *, #14076, .T. ) ;
#14805=( LENGTH_UNIT ( ) NAMED_UNIT ( * ) SI_UNIT ( .MILLI., .METRE. ) );
#14821=ADVANCED_FACE ( 'NONE', ( #2145 ), #5218, .T. ) ;
#14824=CARTESIAN_POINT ( 'NONE',  ( 4.999999999999997335, 0.000000000000000000, 0.000000000000000000 ) ) ;
#14871=CARTESIAN_POINT ( 'NONE',  ( 0.000000000000000000, 5.051668046482832750E-16, -4.000000000000000000 ) ) ;
#14902=CIRCLE ( 'NONE', #11185, 2.041999999999999815 ) ;
#14923=DIRECTION ( 'NONE',  ( -1.000000000000000000, -0.000000000000000000, -0.000000000000000000 ) ) ;
#14962=EDGE_CURVE ( 'NONE', #13015, #6246, #4196, .T. ) ;
#14973=ORIENTED_EDGE ( 'NONE', *, *, #3834, .F. ) ;
#14979=EDGE_LOOP ( 'NONE', ( #15156, #6395, #19527 ) ) ;
#15008=VECTOR ( 'NONE', #19755, 1000.000000000000000 ) ;
#15044=ADVANCED_FACE ( 'NONE', ( #12545 ), #7923, .T. ) ;
#15083=DIRECTION ( 'NONE',  ( 0.000000000000000000, 1.000000000000000000, -1.287488025362403787E-15 ) ) ;
#15087=CARTESIAN_POINT ( 'NONE',  ( 2.500000000000000000, 0.000000000000000000, 0.000000000000000000 ) ) ;
#15114=ORIENTED_EDGE ( 'NONE', *, *, #8846, .F. ) ;
#15156=ORIENTED_EDGE ( 'NONE', *, *, #8842, .T. ) ;
#15192=DIRECTION ( 'NONE',  ( 1.000000000000000000, 0.000000000000000000, 0.000000000000000000 ) ) ;
#15250=ADVANCED_BREP_SHAPE_REPRESENTATION ( '', ( #3497, #12461 ), #2587 ) ;
#15280=ORIENTED_EDGE ( 'NONE', *, *, #10892, .F. ) ;
#15284=DIRECTION ( 'NONE',  ( -1.000000000000000000, -0.000000000000000000, -0.000000000000000000 ) ) ;
#15289=AXIS2_PLACEMENT_3D ( 'NONE', #7327, #7755, #20256 ) ;
#15352=SURFACE_STYLE_FILL_AREA ( #5483 ) ;
#15360=DIRECTION ( 'NONE',  ( -1.000000000000000000, -0.000000000000000000, -0.000000000000000000 ) ) ;
#15462=( NAMED_UNIT ( * ) PLANE_ANGLE_UNIT ( ) SI_UNIT ( $, .RADIAN. ) );
#15469=LINE ( 'NONE', #5808, #11425 ) ;
#15511=DIRECTION ( 'NONE',  ( 0.000000000000000000, 0.000000000000000000, 1.000000000000000000 ) ) ;
#15532=VERTEX_POINT ( 'NONE', #20773 ) ;
#15538=CARTESIAN_POINT ( 'NONE',  ( 2.500000000000000000, 2.357898499370431722, -2.818925648462311528E-15 ) ) ;
#15610=DIRECTION ( 'NONE',  ( -0.000000000000000000, 1.000000000000000000, 1.224646799147353207E-16 ) ) ;
#15614=EDGE_CURVE ( 'NONE', #16659, #11587, #15692, .T. ) ;
#15646=CARTESIAN_POINT ( 'NONE',  ( 21.00000000000000000, 2.055000000000000160, 0.000000000000000000 ) ) ;
#15647=LINE ( 'NONE', #7711, #4616 ) ;
#15689=CARTESIAN_POINT ( 'NONE',  ( 2.500000000000000000, -2.357898499370432166, 3.035766082959412415E-15 ) ) ;
#15692=LINE ( 'NONE', #12740, #5510 ) ;
#15735=EDGE_CURVE ( 'NONE', #19592, #1298, #19389, .T. ) ;
#15833=VERTEX_POINT ( 'NONE', #17819 ) ;
#15853=CARTESIAN_POINT ( 'NONE',  ( 2.500000000000000000, 2.357898499370431722, -2.818925648462311528E-15 ) ) ;
#15863=DIRECTION ( 'NONE',  ( 0.000000000000000000, 0.000000000000000000, -1.000000000000000000 ) ) ;
#15925=DIRECTION ( 'NONE',  ( 0.000000000000000000, 0.000000000000000000, 1.000000000000000000 ) ) ;
#15939=ORIENTED_EDGE ( 'NONE', *, *, #13780, .T. ) ;
#15992=DIRECTION ( 'NONE',  ( -1.000000000000000000, -0.000000000000000000, -0.000000000000000000 ) ) ;
#16008=VECTOR ( 'NONE', #10455, 1000.000000000000000 ) ;
#16026=CIRCLE ( 'NONE', #6868, 0.2000000000000000944 ) ;
#16029=DIRECTION ( 'NONE',  ( 0.000000000000000000, 0.000000000000000000, 1.000000000000000000 ) ) ;
#16061=AXIS2_PLACEMENT_3D ( 'NONE', #14770, #252, #11582 ) ;
#16076=DIRECTION ( 'NONE',  ( 0.000000000000000000, 0.4999999999999990008, -0.8660254037844391517 ) ) ;
#16127=DIRECTION ( 'NONE',  ( -1.000000000000000000, -0.000000000000000000, -0.000000000000000000 ) ) ;
#16131=VERTEX_POINT ( 'NONE', #7054 ) ;
#16137=ORIENTED_EDGE ( 'NONE', *, *, #11453, .T. ) ;
#16138=DIRECTION ( 'NONE',  ( 0.000000000000000000, 0.000000000000000000, 1.000000000000000000 ) ) ;
#16181=FACE_OUTER_BOUND ( 'NONE', #6490, .T. ) ;
#16239=ORIENTED_EDGE ( 'NONE', *, *, #18404, .F. ) ;
#16274=DIRECTION ( 'NONE',  ( 0.000000000000000000, 0.000000000000000000, -1.000000000000000000 ) ) ;
#16323=DIRECTION ( 'NONE',  ( 0.000000000000000000, 0.000000000000000000, 1.000000000000000000 ) ) ;
#16334=VERTEX_POINT ( 'NONE', #9083 ) ;
#16411=ORIENTED_EDGE ( 'NONE', *, *, #8097, .T. ) ;
#16431=DIRECTION ( 'NONE',  ( 0.000000000000000000, 0.000000000000000000, 1.000000000000000000 ) ) ;
#16434=ORIENTED_EDGE ( 'NONE', *, *, #4406, .F. ) ;
#16445=MECHANICAL_DESIGN_GEOMETRIC_PRESENTATION_REPRESENTATION('',(#10021),#12701);
#16489=ADVANCED_FACE ( 'NONE', ( #9707 ), #3237, .T. ) ;
#16539=DIRECTION ( 'NONE',  ( -1.000000000000000000, -0.000000000000000000, -0.000000000000000000 ) ) ;
#16555=LINE ( 'NONE', #5414, #401 ) ;
#16564=EDGE_LOOP ( 'NONE', ( #16931, #9652, #11047, #17897, #14471 ) ) ;
#16659=VERTEX_POINT ( 'NONE', #483 ) ;
#16688=DIRECTION ( 'NONE',  ( 1.000000000000000000, 0.000000000000000000, 0.000000000000000000 ) ) ;
#16693=AXIS2_PLACEMENT_3D ( 'NONE', #4052, #16993, #10533 ) ;
#16716=CARTESIAN_POINT ( 'NONE',  ( 2.500000000000000000, -1.178949249685218748, -2.041999999999998039 ) ) ;
#16732=( LENGTH_UNIT ( ) NAMED_UNIT ( * ) SI_UNIT ( .MILLI., .METRE. ) );
#16754=PRODUCT_DEFINITION_FORMATION_WITH_SPECIFIED_SOURCE ( 'ANY', '', #12039, .NOT_KNOWN. ) ;
#16765=ORIENTED_EDGE ( 'NONE', *, *, #3635, .T. ) ;
#16803=VERTEX_POINT ( 'NONE', #9060 ) ;
#16841=SHAPE_REPRESENTATION_RELATIONSHIP ( 'NONE' , 'NONE' ,  #12383, #15250 ) ;
#16886=CARTESIAN_POINT ( 'NONE',  ( -31.74999999999995737, 0.000000000000000000, 4.250000000000000000 ) ) ;
#16902=ORIENTED_EDGE ( 'NONE', *, *, #15614, .F. ) ;
#16905=CARTESIAN_POINT ( 'NONE',  ( 2.500000000000000000, 2.357898499370431722, -2.818925648462311528E-15 ) ) ;
#16907=CARTESIAN_POINT ( 'NONE',  ( 0.000000000000000000, 0.000000000000000000, 4.000000000000000000 ) ) ;
#16931=ORIENTED_EDGE ( 'NONE', *, *, #5284, .F. ) ;
#16983=PLANE ( 'NONE',  #20143 ) ;
#16993=DIRECTION ( 'NONE',  ( -0.000000000000000000, 1.287488025362403787E-15, 1.000000000000000000 ) ) ;
#16998=ORIENTED_EDGE ( 'NONE', *, *, #13621, .T. ) ;
#17021=CARTESIAN_POINT ( 'NONE',  ( 0.000000000000000000, 1.178949249685212974, -2.042000000000001148 ) ) ;
#17033=CIRCLE ( 'NONE', #7898, 2.700000000000000622 ) ;
#17088=CARTESIAN_POINT ( 'NONE',  ( 21.00000000000000355, 0.000000000000000000, 2.055000000000000160 ) ) ;
#17130=PRODUCT_DEFINITION ( 'UNKNOWN', '', #16754, #20224 ) ;
#17132=FACE_OUTER_BOUND ( 'NONE', #3325, .T. ) ;
#17141=PLANE ( 'NONE',  #10548 ) ;
#17182=DIRECTION ( 'NONE',  ( -0.5000000000000051070, 1.060575238724903217E-16, -0.8660254037844355990 ) ) ;
#17226=ORIENTED_EDGE ( 'NONE', *, *, #10727, .T. ) ;
#17316=CARTESIAN_POINT ( 'NONE',  ( 0.2500000000000002220, 4.898587196589412829E-16, -4.000000000000000000 ) ) ;
#17347=VECTOR ( 'NONE', #196, 1000.000000000000000 ) ;
#17448=CARTESIAN_POINT ( 'NONE',  ( 2.500000000000000000, 0.000000000000000000, 0.000000000000000000 ) ) ;
#17496=ORIENTED_EDGE ( 'NONE', *, *, #13129, .T. ) ;
#17532=AXIS2_PLACEMENT_3D ( 'NONE', #7511, #5932, #12403 ) ;
#17561=CARTESIAN_POINT ( 'NONE',  ( 0.000000000000000000, 0.000000000000000000, 0.000000000000000000 ) ) ;
#17571=FACE_OUTER_BOUND ( 'NONE', #7089, .T. ) ;
#17579=LINE ( 'NONE', #19258, #10342 ) ;
#17594=DIRECTION ( 'NONE',  ( -0.000000000000000000, 0.000000000000000000, 1.000000000000000000 ) ) ;
#17623=FACE_OUTER_BOUND ( 'NONE', #20477, .T. ) ;
#17649=ORIENTED_EDGE ( 'NONE', *, *, #10784, .F. ) ;
#17662=CARTESIAN_POINT ( 'NONE',  ( 2.500000000000000000, -1.178949249685214307, 2.042000000000001592 ) ) ;
#17695=ORIENTED_EDGE ( 'NONE', *, *, #18827, .F. ) ;
#17706=ORIENTED_EDGE ( 'NONE', *, *, #19965, .T. ) ;
#17744=EDGE_LOOP ( 'NONE', ( #19107, #17649, #20673, #1691, #11886 ) ) ;
#17775=DIRECTION ( 'NONE',  ( 0.000000000000000000, 0.000000000000000000, 1.000000000000000000 ) ) ;
#17788=LINE ( 'NONE', #3254, #18873 ) ;
#17810=DIRECTION ( 'NONE',  ( -1.000000000000000000, -0.000000000000000000, -0.000000000000000000 ) ) ;
#17819=CARTESIAN_POINT ( 'NONE',  ( 2.500000000000000000, 2.357898499370431722, -2.818925648462311528E-15 ) ) ;
#17834=ORIENTED_EDGE ( 'NONE', *, *, #15614, .T. ) ;
#17845=VECTOR ( 'NONE', #19717, 1000.000000000000000 ) ;
#17851=VECTOR ( 'NONE', #14923, 1000.000000000000000 ) ;
#17880=DIRECTION ( 'NONE',  ( -1.000000000000000000, -0.000000000000000000, -0.000000000000000000 ) ) ;
#17897=ORIENTED_EDGE ( 'NONE', *, *, #861, .T. ) ;
#17942=LINE ( 'NONE', #9680, #1818 ) ;
#17989=AXIS2_PLACEMENT_3D ( 'NONE', #13653, #5580, #8555 ) ;
#18029=EDGE_LOOP ( 'NONE', ( #747, #2091, #18847, #959, #17706 ) ) ;
#18030=DIRECTION ( 'NONE',  ( -1.000000000000000000, -0.000000000000000000, -0.000000000000000000 ) ) ;
#18159=EDGE_LOOP ( 'NONE', ( #5896, #17834, #16411, #5082, #14800 ) ) ;
#18162=CARTESIAN_POINT ( 'NONE',  ( 2.500000000000000000, 0.000000000000000000, 0.000000000000000000 ) ) ;
#18321=UNCERTAINTY_MEASURE_WITH_UNIT (LENGTH_MEASURE( 1.000000000000000082E-05 ), #13661, 'distance_accuracy_value', 'NONE');
#18329=AXIS2_PLACEMENT_3D ( 'NONE', #19329, #12681, #9280 ) ;
#18404=EDGE_CURVE ( 'NONE', #896, #19670, #20032, .T. ) ;
#18585=LINE ( 'NONE', #18685, #14119 ) ;
#18591=DIRECTION ( 'NONE',  ( 1.000000000000000000, 0.000000000000000000, 0.000000000000000000 ) ) ;
#18617=ORIENTED_EDGE ( 'NONE', *, *, #7015, .F. ) ;
#18641=CARTESIAN_POINT ( 'NONE',  ( 20.55500000000001748, 0.000000000000000000, 0.000000000000000000 ) ) ;
#18645=CARTESIAN_POINT ( 'NONE',  ( 21.00000000000000355, 0.000000000000000000, 0.000000000000000000 ) ) ;
#18685=CARTESIAN_POINT ( 'NONE',  ( -31.74999999999995737, 0.000000000000000000, 2.500000000000000444 ) ) ;
#18722=MECHANICAL_DESIGN_GEOMETRIC_PRESENTATION_REPRESENTATION('',(#2468),#5856);
#18770=DIRECTION ( 'NONE',  ( 0.000000000000000000, 0.000000000000000000, -1.000000000000000000 ) ) ;
#18780=FACE_OUTER_BOUND ( 'NONE', #12873, .T. ) ;
#18791=COLOUR_RGB ( '', 0.09019608, 0.27058824, 0.51372549) ;
#18827=EDGE_CURVE ( 'NONE', #15532, #5814, #1934, .T. ) ;
#18829=AXIS2_PLACEMENT_3D ( 'NONE', #3486, #16127, #16323 ) ;
#18832=DIRECTION ( 'NONE',  ( 0.000000000000000000, -1.000000000000000000, 1.287488025362403787E-15 ) ) ;
#18847=ORIENTED_EDGE ( 'NONE', *, *, #11617, .F. ) ;
#18873=VECTOR ( 'NONE', #74, 1000.000000000000114 ) ;
#18879=ORIENTED_EDGE ( 'NONE', *, *, #4817, .F. ) ;
#18888=DIRECTION ( 'NONE',  ( -0.5000000000000051070, 0.000000000000000000, 0.8660254037844355990 ) ) ;
#18899=FACE_OUTER_BOUND ( 'NONE', #911, .T. ) ;
#18915=ORIENTED_EDGE ( 'NONE', *, *, #11179, .T. ) ;
#18970=ORIENTED_EDGE ( 'NONE', *, *, #12894, .F. ) ;
#18980=ORIENTED_EDGE ( 'NONE', *, *, #20634, .T. ) ;
#18985=DIRECTION ( 'NONE',  ( -1.000000000000000000, -0.000000000000000000, -0.000000000000000000 ) ) ;
#18990=DIRECTION ( 'NONE',  ( 0.000000000000000000, -0.5000000000000009992, -0.8660254037844380415 ) ) ;
#19003=ADVANCED_FACE ( 'NONE', ( #2746 ), #12794, .T. ) ;
#19008=DIRECTION ( 'NONE',  ( -1.000000000000000000, -0.000000000000000000, -0.000000000000000000 ) ) ;
#19085=DIRECTION ( 'NONE',  ( 0.000000000000000000, -0.5000000000000013323, -0.8660254037844380415 ) ) ;
#19107=ORIENTED_EDGE ( 'NONE', *, *, #14150, .T. ) ;
#19172=VECTOR ( 'NONE', #6725, 1000.000000000000000 ) ;
#19177=DIRECTION ( 'NONE',  ( -1.000000000000000000, 0.000000000000000000, -0.000000000000000000 ) ) ;
#19188=AXIS2_PLACEMENT_3D ( 'NONE', #9947, #202, #11642 ) ;
#19222=CIRCLE ( 'NONE', #11765, 2.500000000000000888 ) ;
#19240=DIRECTION ( 'NONE',  ( -1.000000000000000000, -0.000000000000000000, -0.000000000000000000 ) ) ;
#19258=CARTESIAN_POINT ( 'NONE',  ( 0.000000000000000000, 2.357898499370431722, -2.818925648462311528E-15 ) ) ;
#19311=EDGE_CURVE ( 'NONE', #440, #3863, #14693, .T. ) ;
#19329=CARTESIAN_POINT ( 'NONE',  ( 2.500000000000000000, 2.357898499370431722, -2.818925648462311528E-15 ) ) ;
#19389=LINE ( 'NONE', #3586, #2159 ) ;
#19413=VERTEX_POINT ( 'NONE', #19962 ) ;
#19437=DIRECTION ( 'NONE',  ( 0.000000000000000000, 0.000000000000000000, 1.000000000000000000 ) ) ;
#19468=VECTOR ( 'NONE', #14467, 1000.000000000000114 ) ;
#19474=CARTESIAN_POINT ( 'NONE',  ( 0.000000000000000000, 0.000000000000000000, 0.000000000000000000 ) ) ;
#19527=ORIENTED_EDGE ( 'NONE', *, *, #11179, .F. ) ;
#19530=AXIS2_PLACEMENT_3D ( 'NONE', #18645, #12505, #12176 ) ;
#19548=LINE ( 'NONE', #5029, #15008 ) ;
#19588=DIRECTION ( 'NONE',  ( 1.000000000000000000, 0.000000000000000000, 0.000000000000000000 ) ) ;
#19592=VERTEX_POINT ( 'NONE', #6081 ) ;
#19670=VERTEX_POINT ( 'NONE', #10100 ) ;
#19681=AXIS2_PLACEMENT_3D ( 'NONE', #17448, #19240, #20610 ) ;
#19691=VERTEX_POINT ( 'NONE', #14871 ) ;
#19717=DIRECTION ( 'NONE',  ( -1.000000000000000000, -0.000000000000000000, -0.000000000000000000 ) ) ;
#19723=CIRCLE ( 'NONE', #20730, 4.250000000000000000 ) ;
#19745=FACE_OUTER_BOUND ( 'NONE', #3197, .T. ) ;
#19754=ADVANCED_FACE ( 'NONE', ( #12725 ), #1179, .F. ) ;
#19755=DIRECTION ( 'NONE',  ( -1.000000000000000000, -0.000000000000000000, -0.000000000000000000 ) ) ;
#19820=ORIENTED_EDGE ( 'NONE', *, *, #1580, .F. ) ;
#19836=DIRECTION ( 'NONE',  ( -0.7071067811865364705, 0.000000000000000000, 0.7071067811865584529 ) ) ;
#19837=CARTESIAN_POINT ( 'NONE',  ( -31.74999999999995737, 0.000000000000000000, 0.000000000000000000 ) ) ;
#19847=DIRECTION ( 'NONE',  ( 0.000000000000000000, 1.224646799147353207E-16, 1.000000000000000000 ) ) ;
#19861=CARTESIAN_POINT ( 'NONE',  ( 0.000000000000000000, 1.178949249685212974, -2.042000000000001148 ) ) ;
#19880=FILL_AREA_STYLE ('',( #5041 ) ) ;
#19925=CARTESIAN_POINT ( 'NONE',  ( 5.200000000000002842, 0.000000000000000000, 2.500000000000000444 ) ) ;
#19934=LINE ( 'NONE', #7213, #3835 ) ;
#19962=CARTESIAN_POINT ( 'NONE',  ( 4.999999999999997335, 0.000000000000000000, 4.250000000000000000 ) ) ;
#19965=EDGE_CURVE ( 'NONE', #510, #16131, #617, .T. ) ;
#20031=CARTESIAN_POINT ( 'NONE',  ( 0.2500000000000002220, 0.000000000000000000, 4.000000000000000000 ) ) ;
#20032=LINE ( 'NONE', #5727, #11198 ) ;
#20140=DIRECTION ( 'NONE',  ( 0.000000000000000000, 0.4999999999999990008, -0.8660254037844391517 ) ) ;
#20143=AXIS2_PLACEMENT_3D ( 'NONE', #2470, #8933, #20267 ) ;
#20163=CARTESIAN_POINT ( 'NONE',  ( 5.000000000000000888, 0.000000000000000000, 0.000000000000000000 ) ) ;
#20167=VECTOR ( 'NONE', #13105, 1000.000000000000114 ) ;
#20213=CIRCLE ( 'NONE', #12455, 4.000000000000000000 ) ;
#20224=PRODUCT_DEFINITION_CONTEXT ( 'detailed design', #12920, 'design' ) ;
#20256=DIRECTION ( 'NONE',  ( 0.000000000000000000, 0.000000000000000000, -1.000000000000000000 ) ) ;
#20267=DIRECTION ( 'NONE',  ( 0.000000000000000000, 0.4999999999999992784, -0.8660254037844389297 ) ) ;
#20273=ORIENTED_EDGE ( 'NONE', *, *, #9365, .T. ) ;
#20323=DIRECTION ( 'NONE',  ( 0.000000000000000000, 0.000000000000000000, 1.000000000000000000 ) ) ;
#20459=VERTEX_POINT ( 'NONE', #11720 ) ;
#20477=EDGE_LOOP ( 'NONE', ( #1314, #248, #6382, #13020, #7339 ) ) ;
#20488=CARTESIAN_POINT ( 'NONE',  ( 21.00000000000000355, 0.000000000000000000, 0.000000000000000000 ) ) ;
#20491=DIRECTION ( 'NONE',  ( 0.000000000000000000, -1.224646799147353454E-16, 1.000000000000000000 ) ) ;
#20610=DIRECTION ( 'NONE',  ( 0.000000000000000000, 0.000000000000000000, 1.000000000000000000 ) ) ;
#20626=EDGE_CURVE ( 'NONE', #19670, #3863, #19222, .T. ) ;
#20634=EDGE_CURVE ( 'NONE', #1298, #540, #15469, .T. ) ;
#20673=ORIENTED_EDGE ( 'NONE', *, *, #15735, .F. ) ;
#20693=LINE ( 'NONE', #3106, #19468 ) ;
#20730=AXIS2_PLACEMENT_3D ( 'NONE', #9523, #15992, #1493 ) ;
#20773=CARTESIAN_POINT ( 'NONE',  ( 5.200000000000002842, 3.061616997868383634E-16, -2.500000000000000444 ) ) ;
#20812=CARTESIAN_POINT ( 'NONE',  ( 2.500000000000000000, -2.357898499370432166, 3.035766082959412415E-15 ) ) ;
#20833=CYLINDRICAL_SURFACE ( 'NONE', #6808, 4.250000000000000000 ) ;
#20923=ORIENTED_EDGE ( 'NONE', *, *, #4433, .F. ) ;
ENDSEC;
END-ISO-10303-21;
